ISO-10303-21;
HEADER;
FILE_DESCRIPTION (('STEP AP214'),
    '1' );
FILE_NAME ('Socket Head Cap Screw.step',
    '2026-10-09T10:51:02',
    ( '' ),
    ( '' ),
    'SwSTEP 2.0',
    'SolidWorks 2026',
    '' );
FILE_SCHEMA (( 'AUTOMOTIVE_DESIGN' ));
ENDSEC;

DATA;
#15=CARTESIAN_POINT ( 'NONE',  ( -41.94137166082473556, 162.5796238295972671, 273.2086669205137355 ) ) ;
#30=DIRECTION ( 'NONE',  ( 0.9909299940865187173, -0.1338359446631173233, -0.01207007604876291287 ) ) ;
#73=CARTESIAN_POINT ( 'NONE',  ( -37.87284078821844702, 165.3754468158257112, 244.8283704289042362 ) ) ;
#123=AXIS2_PLACEMENT_3D ( 'NONE', #888, #21632, #12956 ) ;
#134=VERTEX_POINT ( 'NONE', #1493 ) ;
#147=DIRECTION ( 'NONE',  ( 0.9909299940865187173, -0.1338359446631173233, -0.01207007604876291287 ) ) ;
#156=CARTESIAN_POINT ( 'NONE',  ( -44.49054948644865703, 166.4747265717734308, 273.2201396957804036 ) ) ;
#160=VERTEX_POINT ( 'NONE', #21115 ) ;
#179=CARTESIAN_POINT ( 'NONE',  ( -41.52755568966412625, 166.0426042274538077, 268.7837904884077034 ) ) ;
#199=DIRECTION ( 'NONE',  ( 0.01292394549866734098, 0.005513023399720419666, 0.9999012842304692006 ) ) ;
#270=ORIENTED_EDGE ( 'NONE', *, *, #14726, .F. ) ;
#281=DIRECTION ( 'NONE',  ( -0.01292394549866733230, -0.005513023399720419666, -0.9999012842304692006 ) ) ;
#320=CARTESIAN_POINT ( 'NONE',  ( -41.47069032946998846, 166.0668615304125808, 273.1833561390217824 ) ) ;
#348=AXIS2_PLACEMENT_3D ( 'NONE', #1799, #199, #10640 ) ;
#361=CARTESIAN_POINT ( 'NONE',  ( -44.25520882077128704, 168.2183454221810734, 273.2074843050344271 ) ) ;
#391=DIRECTION ( 'NONE',  ( -0.3796287383013210448, 0.9251388995215469313, -0.0001940304313831171454 ) ) ;
#402=VECTOR ( 'NONE', #14560, 999.9999999999998863 ) ;
#416=VECTOR ( 'NONE', #1504, 1000.000000000000000 ) ;
#426=FACE_OUTER_BOUND ( 'NONE', #5369, .T. ) ;
#437=ADVANCED_FACE ( 'NONE', ( #9069 ), #20844, .T. ) ;
#438=FACE_OUTER_BOUND ( 'NONE', #17946, .T. ) ;
#459=CARTESIAN_POINT ( 'NONE',  ( -41.40281863702377052, 169.1866591894303440, 244.1624146268972595 ) ) ;
#500=AXIS2_PLACEMENT_3D ( 'NONE', #6152, #992, #21857 ) ;
#579=DIRECTION ( 'NONE',  ( -0.1337561903331544455, -0.9909881666746205298, 0.007192708699472569189 ) ) ;
#731=CIRCLE ( 'NONE', #19768, 4.400000000000000355 ) ;
#735=CARTESIAN_POINT ( 'NONE',  ( -38.45083117249132698, 165.6589964890517308, 273.1465725822631612 ) ) ;
#742=EDGE_CURVE ( 'NONE', #12084, #21410, #8941, .T. ) ;
#751=PRODUCT_DEFINITION_SHAPE ( 'NONE', 'NONE',  #21773 ) ;
#816=AXIS2_PLACEMENT_3D ( 'NONE', #13369, #20347, #10018 ) ;
#832=EDGE_CURVE ( 'NONE', #11858, #8665, #20065, .T. ) ;
#888=CARTESIAN_POINT ( 'NONE',  ( -41.94137166082473556, 162.5796238295972671, 273.2086669205137355 ) ) ;
#948=DIRECTION ( 'NONE',  ( 0.9909299940865190504, -0.1338359446631136318, -0.01207007604876911971 ) ) ;
#950=DIRECTION ( 'NONE',  ( 0.01292394549866733230, 0.005513023399720419666, 0.9999012842304692006 ) ) ;
#964=EDGE_CURVE ( 'NONE', #2284, #160, #4657, .T. ) ;
#968=DIRECTION ( 'NONE',  ( 0.01292394549866733404, 0.005513023399720420534, 0.9999012842304693116 ) ) ;
#980=CARTESIAN_POINT ( 'NONE',  ( -45.88764766364480607, 166.6314823839715302, 268.8368988230222953 ) ) ;
#992=DIRECTION ( 'NONE',  ( -0.01292394549866734098, -0.005513023399720419666, -0.9999012842304692006 ) ) ;
#1054=ORIENTED_EDGE ( 'NONE', *, *, #15435, .T. ) ;
#1188=CIRCLE ( 'NONE', #15492, 0.3999999999999989120 ) ;
#1196=FACE_OUTER_BOUND ( 'NONE', #21190, .T. ) ;
#1212=VECTOR ( 'NONE', #13349, 999.9999999999998863 ) ;
#1222=AXIS2_PLACEMENT_3D ( 'NONE', #4307, #11677, #20277 ) ;
#1229=CARTESIAN_POINT ( 'NONE',  ( -37.16229413748396837, 165.4559312802959994, 269.1306426674853469 ) ) ;
#1242=LINE ( 'NONE', #7987, #18460 ) ;
#1329=EDGE_LOOP ( 'NONE', ( #16290, #11373, #17539, #13804, #17308 ) ) ;
#1363=EDGE_CURVE ( 'NONE', #134, #18610, #14624, .T. ) ;
#1371=DIRECTION ( 'NONE',  ( 0.01292394549866733404, 0.005513023399720420534, 0.9999012842304693116 ) ) ;
#1382=DIRECTION ( 'NONE',  ( 0.01292394549866733230, 0.005513023399720419666, 0.9999012842304692006 ) ) ;
#1395=DIRECTION ( 'NONE',  ( 1.000000000000000000, 0.000000000000000000, 0.000000000000000000 ) ) ;
#1416=DIRECTION ( 'NONE',  ( -0.01292394549866733230, -0.005513023399720419666, -0.9999012842304692006 ) ) ;
#1423=VERTEX_POINT ( 'NONE', #11622 ) ;
#1460=ORIENTED_EDGE ( 'NONE', *, *, #7680, .T. ) ;
#1466=DIRECTION ( 'NONE',  ( 0.01292394549866734098, 0.005513023399720419666, 0.9999012842304692006 ) ) ;
#1488=CARTESIAN_POINT ( 'NONE',  ( -41.47069032946998846, 166.0668615304125808, 273.1833561390217824 ) ) ;
#1493=CARTESIAN_POINT ( 'NONE',  ( -45.88247808544533513, 166.6336875933314161, 269.2368593367144740 ) ) ;
#1504=DIRECTION ( 'NONE',  ( 0.7912924530843117310, -0.6113994113550570431, -0.006856638134102506846 ) ) ;
#1620=CARTESIAN_POINT ( 'NONE',  ( -40.31377174949672337, 163.2475007341206776, 273.1839474467614650 ) ) ;
#1657=EDGE_CURVE ( 'NONE', #18197, #21410, #21895, .T. ) ;
#1669=LINE ( 'NONE', #7270, #16480 ) ;
#1695=EDGE_CURVE ( 'NONE', #20021, #12292, #10809, .T. ) ;
#1700=CARTESIAN_POINT ( 'NONE',  ( -39.60774975246459917, 168.4783572853436624, 273.1459812745235354 ) ) ;
#1707=CARTESIAN_POINT ( 'NONE',  ( -41.84548474893134085, 165.9069838518206836, 244.1862188963381755 ) ) ;
#1743=LINE ( 'NONE', #3677, #16966 ) ;
#1744=DIRECTION ( 'NONE',  ( 0.9909299940865187173, -0.1338359446631173233, -0.01207007604876291287 ) ) ;
#1799=CARTESIAN_POINT ( 'NONE',  ( -38.21549050681395698, 167.4026153394593734, 273.1339171915171846 ) ) ;
#1810=VERTEX_POINT ( 'NONE', #73 ) ;
#1824=DIRECTION ( 'NONE',  ( 0.9909299940865190504, -0.1338359446631136318, -0.01207007604876911971 ) ) ;
#1834=CARTESIAN_POINT ( 'NONE',  ( -42.62760890944326775, 168.8862223267045124, 273.1827648312820997 ) ) ;
#1850=AXIS2_PLACEMENT_3D ( 'NONE', #2128, #21419, #5679 ) ;
#1878=CARTESIAN_POINT ( 'NONE',  ( -41.41899454747532161, 166.0889136240114681, 277.1829612759436827 ) ) ;
#1915=MANIFOLD_SOLID_BREP ( 'Stock-MAS-425-1', #16147 ) ;
#1924=CONICAL_SURFACE ( 'NONE', #13673, 3.309500000000002107, 0.7853981633974710386 ) ;
#1992=LINE ( 'NONE', #156, #21366 ) ;
#2056=EDGE_CURVE ( 'NONE', #12292, #4350, #1669, .T. ) ;
#2092=FACE_BOUND ( 'NONE', #12857, .T. ) ;
#2097=FACE_OUTER_BOUND ( 'NONE', #4084, .T. ) ;
#2128=CARTESIAN_POINT ( 'NONE',  ( -41.52755568966412625, 166.0426042274538077, 268.7837904884077034 ) ) ;
#2135=ORIENTED_EDGE ( 'NONE', *, *, #5396, .T. ) ;
#2183=ORIENTED_EDGE ( 'NONE', *, *, #15429, .F. ) ;
#2217=ORIENTED_EDGE ( 'NONE', *, *, #964, .T. ) ;
#2253=DIRECTION ( 'NONE',  ( -0.9909299940865190504, 0.1338359446631142147, 0.01207007604876868083 ) ) ;
#2284=VERTEX_POINT ( 'NONE', #10846 ) ;
#2306=ORIENTED_EDGE ( 'NONE', *, *, #22096, .F. ) ;
#2308=CARTESIAN_POINT ( 'NONE',  ( -38.63447605617402303, 163.9374297322429470, 277.1588331099309812 ) ) ;
#2363=ORIENTED_EDGE ( 'NONE', *, *, #7383, .T. ) ;
#2365=EDGE_CURVE ( 'NONE', #6708, #5718, #20563, .T. ) ;
#2378=FACE_OUTER_BOUND ( 'NONE', #20923, .T. ) ;
#2391=CIRCLE ( 'NONE', #8251, 3.047499999999998987 ) ;
#2400=EDGE_CURVE ( 'NONE', #1810, #13772, #4705, .T. ) ;
#2436=FACE_OUTER_BOUND ( 'NONE', #18984, .T. ) ;
#2468=CARTESIAN_POINT ( 'NONE',  ( -41.52755568966412625, 166.0426042274538077, 268.7837904884077034 ) ) ;
#2501=MECHANICAL_DESIGN_GEOMETRIC_PRESENTATION_REPRESENTATION('',(#4684),#16104);
#2572=ORIENTED_EDGE ( 'NONE', *, *, #2056, .F. ) ;
#2591=EDGE_CURVE ( 'NONE', #21410, #20004, #9178, .T. ) ;
#2594=DIRECTION ( 'NONE',  ( 0.9909299940865187173, -0.1338359446631179062, -0.01207007604876208194 ) ) ;
#2597=AXIS2_PLACEMENT_3D ( 'NONE', #1707, #17111, #10437 ) ;
#2614=EDGE_LOOP ( 'NONE', ( #10124, #11575, #13917, #20807, #7880 ) ) ;
#2619=VECTOR ( 'NONE', #13602, 1000.000000000000114 ) ;
#2651=ORIENTED_EDGE ( 'NONE', *, *, #16711, .T. ) ;
#2684=AXIS2_PLACEMENT_3D ( 'NONE', #7324, #14136, #21114 ) ;
#2763=EDGE_CURVE ( 'NONE', #7115, #14816, #22016, .T. ) ;
#2808=DIRECTION ( 'NONE',  ( 0.9910138020846641638, -0.1337596504095987238, 0.000000000000000000 ) ) ;
#2818=CARTESIAN_POINT ( 'NONE',  ( -34.98828874231188735, 165.2145695649813888, 276.3045847542423417 ) ) ;
#2820=FACE_OUTER_BOUND ( 'NONE', #11515, .T. ) ;
#2822=ORIENTED_EDGE ( 'NONE', *, *, #16123, .F. ) ;
#2826=CARTESIAN_POINT ( 'NONE',  ( -41.00865927789263310, 166.2639521169525665, 308.9298270502609967 ) ) ;
#2829=FACE_OUTER_BOUND ( 'NONE', #2614, .T. ) ;
#2887=ORIENTED_EDGE ( 'NONE', *, *, #2763, .F. ) ;
#2894=EDGE_CURVE ( 'NONE', #18513, #3984, #17596, .T. ) ;
#2900=CARTESIAN_POINT ( 'NONE',  ( -38.21549050681395698, 167.4026153394593734, 273.1339171915171846 ) ) ;
#2932=CONICAL_SURFACE ( 'NONE', #15799, 5.700000000000001954, 0.7853981633974482790 ) ;
#2942=ORIENTED_EDGE ( 'NONE', *, *, #1657, .F. ) ;
#2976=VECTOR ( 'NONE', #18954, 1000.000000000000227 ) ;
#3102=CARTESIAN_POINT ( 'NONE',  ( 0.000000000000000000, 0.000000000000000000, 0.000000000000000000 ) ) ;
#3106=FACE_OUTER_BOUND ( 'NONE', #10728, .T. ) ;
#3226=ORIENTED_EDGE ( 'NONE', *, *, #3870, .F. ) ;
#3272=VECTOR ( 'NONE', #9548, 1000.000000000000227 ) ;
#3299=ORIENTED_EDGE ( 'NONE', *, *, #2591, .F. ) ;
#3317=DIRECTION ( 'NONE',  ( 0.01292394549866733230, 0.005513023399720419666, 0.9999012842304692006 ) ) ;
#3323=ORIENTED_EDGE ( 'NONE', *, *, #17252, .F. ) ;
#3443=EDGE_LOOP ( 'NONE', ( #6648, #12270, #7216, #8861 ) ) ;
#3467=AXIS2_PLACEMENT_3D ( 'NONE', #22122, #6523, #15614 ) ;
#3506=DIRECTION ( 'NONE',  ( 0.01292394549866733230, 0.005513023399720419666, 0.9999012842304692006 ) ) ;
#3519=PLANE ( 'NONE',  #348 ) ;
#3520=ORIENTED_EDGE ( 'NONE', *, *, #11394, .F. ) ;
#3542=DIRECTION ( 'NONE',  ( 0.01292394549866733230, 0.005513023399720419666, 0.9999012842304692006 ) ) ;
#3567=ORIENTED_EDGE ( 'NONE', *, *, #15857, .T. ) ;
#3570=CARTESIAN_POINT ( 'NONE',  ( -41.83656076456451700, 165.9107905944781862, 244.8766507330992681 ) ) ;
#3610=EDGE_CURVE ( 'NONE', #160, #3984, #6107, .T. ) ;
#3677=CARTESIAN_POINT ( 'NONE',  ( -41.88967587883006871, 162.6016759231961260, 277.2082720574355790 ) ) ;
#3723=ADVANCED_FACE ( 'NONE', ( #5999 ), #20104, .T. ) ;
#3730=CARTESIAN_POINT ( 'NONE',  ( -41.52238611146465530, 166.0448094368136935, 269.1837510020998820 ) ) ;
#3753=VECTOR ( 'NONE', #13380, 1000.000000000000227 ) ;
#3763=DIRECTION ( 'NONE',  ( 0.01292394549866733230, 0.005513023399720419666, 0.9999012842304692006 ) ) ;
#3771=EDGE_CURVE ( 'NONE', #7184, #17163, #10943, .T. ) ;
#3837=DIRECTION ( 'NONE',  ( 0.9250486434174661765, 0.3795887553195633202, -0.01404934683357507604 ) ) ;
#3857=PRESENTATION_STYLE_ASSIGNMENT (( #19585 ) ) ;
#3870=EDGE_CURVE ( 'NONE', #18167, #12292, #22291, .T. ) ;
#3889=EDGE_LOOP ( 'NONE', ( #10296, #14339, #7819, #3948 ) ) ;
#3905=ORIENTED_EDGE ( 'NONE', *, *, #5439, .T. ) ;
#3936=DIRECTION ( 'NONE',  ( -0.01292394549866733230, -0.005513023399720419666, -0.9999012842304692006 ) ) ;
#3948=ORIENTED_EDGE ( 'NONE', *, *, #14878, .T. ) ;
#3957=ORIENTED_EDGE ( 'NONE', *, *, #10582, .F. ) ;
#3984=VERTEX_POINT ( 'NONE', #7286 ) ;
#4012=ADVANCED_FACE ( 'NONE', ( #16170 ), #7410, .F. ) ;
#4016=AXIS2_PLACEMENT_3D ( 'NONE', #179, #281, #5209 ) ;
#4078=ORIENTED_EDGE ( 'NONE', *, *, #19331, .T. ) ;
#4084=EDGE_LOOP ( 'NONE', ( #16353, #17998, #8300 ) ) ;
#4085=VECTOR ( 'NONE', #15757, 1000.000000000000114 ) ;
#4117=ADVANCED_FACE ( 'NONE', ( #4183 ), #5428, .F. ) ;
#4183=FACE_OUTER_BOUND ( 'NONE', #14885, .T. ) ;
#4199=FACE_OUTER_BOUND ( 'NONE', #10592, .T. ) ;
#4224=ORIENTED_EDGE ( 'NONE', *, *, #19331, .F. ) ;
#4232=ORIENTED_EDGE ( 'NONE', *, *, #2400, .T. ) ;
#4270=ADVANCED_FACE ( 'NONE', ( #18534 ), #7854, .T. ) ;
#4294=CYLINDRICAL_SURFACE ( 'NONE', #13320, 6.500000000000000000 ) ;
#4307=CARTESIAN_POINT ( 'NONE',  ( -38.21549050681395698, 167.4026153394593734, 273.1339171915171846 ) ) ;
#4350=VERTEX_POINT ( 'NONE', #4712 ) ;
#4439=CIRCLE ( 'NONE', #10323, 0.3999999999999989120 ) ;
#4477=DIRECTION ( 'NONE',  ( -0.9250486434174662875, -0.3795887553195633202, 0.01404934683357507604 ) ) ;
#4493=ORIENTED_EDGE ( 'NONE', *, *, #1363, .T. ) ;
#4547=ORIENTED_EDGE ( 'NONE', *, *, #14878, .F. ) ;
#4555=DIRECTION ( 'NONE',  ( 0.8646325210002208106, -0.1131488163178875073, 0.4894976496313986902 ) ) ;
#4575=CARTESIAN_POINT ( 'NONE',  ( -44.20351303877662019, 168.2403975157799607, 277.2070894419563274 ) ) ;
#4626=CARTESIAN_POINT ( 'NONE',  ( -38.63447605617402303, 163.9374297322429470, 277.1588331099309812 ) ) ;
#4647=DIRECTION ( 'NONE',  ( 0.01292394549866733404, 0.005513023399720420534, 0.9999012842304693116 ) ) ;
#4653=CARTESIAN_POINT ( 'NONE',  ( -41.47069032946998846, 166.0668615304125808, 273.1833561390217824 ) ) ;
#4657=CIRCLE ( 'NONE', #13852, 6.500000000000000000 ) ;
#4684=STYLED_ITEM ( 'NONE', ( #3857 ), #1915 ) ;
#4705=LINE ( 'NONE', #18853, #10957 ) ;
#4712=CARTESIAN_POINT ( 'NONE',  ( -44.72589015212603414, 164.7311077213657597, 273.2327950865263801 ) ) ;
#4717=CARTESIAN_POINT ( 'NONE',  ( -38.68617183816869698, 163.9153776386440882, 273.1592279730091377 ) ) ;
#4744=FACE_OUTER_BOUND ( 'NONE', #3889, .T. ) ;
#4808=ORIENTED_EDGE ( 'NONE', *, *, #13595, .T. ) ;
#4885=AXIS2_PLACEMENT_3D ( 'NONE', #18779, #3936, #7390 ) ;
#4973=ADVANCED_FACE ( 'NONE', ( #426 ), #3519, .T. ) ;
#4984=EDGE_CURVE ( 'NONE', #18610, #134, #731, .T. ) ;
#4999=DIRECTION ( 'NONE',  ( 0.9909299940865187173, -0.1338359446631173233, -0.01207007604876291287 ) ) ;
#5008=ORIENTED_EDGE ( 'NONE', *, *, #12494, .F. ) ;
#5062=PLANE ( 'NONE',  #19502 ) ;
#5137=ORIENTED_EDGE ( 'NONE', *, *, #2763, .T. ) ;
#5171=AXIS2_PLACEMENT_3D ( 'NONE', #7648, #391, #3837 ) ;
#5209=DIRECTION ( 'NONE',  ( -0.9909299940865188283, 0.1338359446631173788, 0.01207007604876290420 ) ) ;
#5369=EDGE_LOOP ( 'NONE', ( #3226, #2651, #13058 ) ) ;
#5396=EDGE_CURVE ( 'NONE', #6708, #18167, #22154, .T. ) ;
#5426=CARTESIAN_POINT ( 'NONE',  ( -45.12496756436068068, 166.3499139106832558, 244.2261648130215690 ) ) ;
#5428=TOROIDAL_SURFACE ( 'NONE', #19384, 4.400000000000000355, 0.4000000000000000222 ) ;
#5439=EDGE_CURVE ( 'NONE', #18197, #11858, #21917, .T. ) ;
#5495=VECTOR ( 'NONE', #18210, 1000.000000000000000 ) ;
#5496=ORIENTED_EDGE ( 'NONE', *, *, #964, .F. ) ;
#5548=DIRECTION ( 'NONE',  ( 0.9909299940865187173, -0.1338359446631173233, -0.01207007604876291287 ) ) ;
#5571=SURFACE_STYLE_FILL_AREA ( #14332 ) ;
#5616=CARTESIAN_POINT ( 'NONE',  ( -44.25520882077128704, 168.2183454221810734, 273.2074843050344271 ) ) ;
#5618=CONICAL_SURFACE ( 'NONE', #4885, 5.700000000000001954, 0.7853981633974482790 ) ;
#5679=DIRECTION ( 'NONE',  ( -0.9909299940865188283, 0.1338359446631172955, 0.01207007604876741101 ) ) ;
#5714=CARTESIAN_POINT ( 'NONE',  ( -41.94137166082473556, 162.5796238295972671, 273.2086669205137355 ) ) ;
#5716=ADVANCED_FACE ( 'NONE', ( #6521 ), #12033, .T. ) ;
#5718=VERTEX_POINT ( 'NONE', #1700 ) ;
#5735=LINE ( 'NONE', #15, #22424 ) ;
#5790=CARTESIAN_POINT ( 'NONE',  ( -38.56600193350200811, 165.4640537929580830, 244.1462729796548103 ) ) ;
#5854=LINE ( 'NONE', #18176, #15507 ) ;
#5914=AXIS2_PLACEMENT_3D ( 'NONE', #1878, #8740, #19214 ) ;
#5952=ORIENTED_EDGE ( 'NONE', *, *, #21158, .F. ) ;
#5999=FACE_OUTER_BOUND ( 'NONE', #19688, .T. ) ;
#6003=AXIS2_PLACEMENT_3D ( 'NONE', #12379, #17435, #19358 ) ;
#6028=ORIENTED_EDGE ( 'NONE', *, *, #7366, .T. ) ;
#6093=DIRECTION ( 'NONE',  ( 0.01292394549866733230, 0.005513023399720419666, 0.9999012842304692006 ) ) ;
#6107=LINE ( 'NONE', #18194, #10200 ) ;
#6116=ORIENTED_EDGE ( 'NONE', *, *, #1695, .F. ) ;
#6150=FACE_OUTER_BOUND ( 'NONE', #17976, .T. ) ;
#6152=CARTESIAN_POINT ( 'NONE',  ( -40.65297087429915024, 172.4862325201987403, 269.1369983955533485 ) ) ;
#6209=CARTESIAN_POINT ( 'NONE',  ( -38.68617183816869698, 163.9153776386440882, 273.1592279730091377 ) ) ;
#6290=ORIENTED_EDGE ( 'NONE', *, *, #3610, .T. ) ;
#6292=AXIS2_PLACEMENT_3D ( 'NONE', #3102, #12069, #1395 ) ;
#6351=CYLINDRICAL_SURFACE ( 'NONE', #816, 4.000000000000002665 ) ;
#6362=LINE ( 'NONE', #4717, #15569 ) ;
#6403=CARTESIAN_POINT ( 'NONE',  ( -43.33363090647537774, 163.6553657754814992, 273.2207310035200294 ) ) ;
#6464=DIRECTION ( 'NONE',  ( 0.01292394549866733404, 0.005513023399720420534, 0.9999012842304693116 ) ) ;
#6470=PLANE ( 'NONE',  #7042 ) ;
#6472=CARTESIAN_POINT ( 'NONE',  ( -35.77069358118214382, 165.3260487394316840, 277.1141618424657054 ) ) ;
#6476=ORIENTED_EDGE ( 'NONE', *, *, #742, .T. ) ;
#6521=FACE_OUTER_BOUND ( 'NONE', #21886, .T. ) ;
#6523=DIRECTION ( 'NONE',  ( 0.01292394549866733230, 0.005513023399720419666, 0.9999012842304692006 ) ) ;
#6549=CARTESIAN_POINT ( 'NONE',  ( -40.94831321612058161, 169.5761513248267818, 277.1576504944517296 ) ) ;
#6560=CARTESIAN_POINT ( 'NONE',  ( -41.41899454747532161, 166.0889136240114681, 277.1829612759436827 ) ) ;
#6570=DIRECTION ( 'NONE',  ( 0.01292394549866733230, 0.005513023399720419666, 0.9999012842304692006 ) ) ;
#6644=CARTESIAN_POINT ( 'NONE',  ( -41.42933370387425640, 166.0845032052916963, 276.3830402485593254 ) ) ;
#6648=ORIENTED_EDGE ( 'NONE', *, *, #21670, .F. ) ;
#6682=CARTESIAN_POINT ( 'NONE',  ( -41.52755568966412625, 166.0426042274538077, 268.7837904884077034 ) ) ;
#6708=VERTEX_POINT ( 'NONE', #15728 ) ;
#6717=EDGE_CURVE ( 'NONE', #4350, #12640, #10432, .T. ) ;
#6875=ORIENTED_EDGE ( 'NONE', *, *, #21670, .T. ) ;
#6990=ORIENTED_EDGE ( 'NONE', *, *, #2365, .F. ) ;
#7016=( GEOMETRIC_REPRESENTATION_CONTEXT ( 3 ) GLOBAL_UNCERTAINTY_ASSIGNED_CONTEXT ( ( #21677 ) ) GLOBAL_UNIT_ASSIGNED_CONTEXT ( ( #19171, #14026, #12649 ) ) REPRESENTATION_CONTEXT ( 'NONE', 'WORKASPACE' ) );
#7018=EDGE_LOOP ( 'NONE', ( #2306, #6990, #2135 ) ) ;
#7020=DIRECTION ( 'NONE',  ( 0.01292394549866733404, 0.005513023399720420534, 0.9999012842304693116 ) ) ;
#7042=AXIS2_PLACEMENT_3D ( 'NONE', #13481, #12212, #1744 ) ;
#7074=EDGE_CURVE ( 'NONE', #8665, #4350, #13190, .T. ) ;
#7079=ORIENTED_EDGE ( 'NONE', *, *, #18193, .F. ) ;
#7098=ADVANCED_FACE ( 'NONE', ( #2829 ), #14929, .F. ) ;
#7115=VERTEX_POINT ( 'NONE', #5426 ) ;
#7132=AXIS2_PLACEMENT_3D ( 'NONE', #2826, #18234, #7769 ) ;
#7159=ORIENTED_EDGE ( 'NONE', *, *, #15484, .T. ) ;
#7184=VERTEX_POINT ( 'NONE', #16270 ) ;
#7194=DIRECTION ( 'NONE',  ( 0.01292394549866733230, 0.005513023399720419666, 0.9999012842304692006 ) ) ;
#7216=ORIENTED_EDGE ( 'NONE', *, *, #9207, .T. ) ;
#7240=ORIENTED_EDGE ( 'NONE', *, *, #15857, .F. ) ;
#7270=CARTESIAN_POINT ( 'NONE',  ( -44.25520882077128704, 168.2183454221810734, 273.2074843050344271 ) ) ;
#7286=CARTESIAN_POINT ( 'NONE',  ( -47.87037866543662545, 166.9544368456019470, 276.4614957428762523 ) ) ;
#7293=FILL_AREA_STYLE_COLOUR ( '', #8351 ) ;
#7296=CARTESIAN_POINT ( 'NONE',  ( -38.68617183816869698, 163.9153776386440882, 273.1592279730091377 ) ) ;
#7306=ADVANCED_FACE ( 'NONE', ( #1196 ), #6470, .T. ) ;
#7324=CARTESIAN_POINT ( 'NONE',  ( -41.84548474893134085, 165.9069838518206836, 244.1862188963381755 ) ) ;
#7366=EDGE_CURVE ( 'NONE', #12349, #13772, #19861, .T. ) ;
#7383=EDGE_CURVE ( 'NONE', #14816, #1810, #16258, .T. ) ;
#7390=DIRECTION ( 'NONE',  ( -0.9909299940865186063, 0.1338359446631179339, 0.01207007604875938098 ) ) ;
#7410=PLANE ( 'NONE',  #12421 ) ;
#7414=CARTESIAN_POINT ( 'NONE',  ( -44.97237925423871019, 166.7992958956050416, 308.9781073544560854 ) ) ;
#7500=DIRECTION ( 'NONE',  ( -0.7912924530843117310, 0.6113994113550570431, 0.006856638134102506846 ) ) ;
#7560=ORIENTED_EDGE ( 'NONE', *, *, #15429, .T. ) ;
#7617=EDGE_LOOP ( 'NONE', ( #2942, #4224, #6476 ) ) ;
#7623=VECTOR ( 'NONE', #579, 1000.000000000000000 ) ;
#7633=DIRECTION ( 'NONE',  ( 0.9909299940865186063, -0.1338359446631180727, -0.01207007604876311237 ) ) ;
#7648=CARTESIAN_POINT ( 'NONE',  ( -41.00000899811524846, 169.5540992312279229, 273.1580453575298293 ) ) ;
#7649=EDGE_CURVE ( 'NONE', #17163, #18513, #5854, .T. ) ;
#7680=EDGE_CURVE ( 'NONE', #20021, #14769, #16119, .T. ) ;
#7728=AXIS2_PLACEMENT_3D ( 'NONE', #9197, #12552, #147 ) ;
#7730=ORIENTED_EDGE ( 'NONE', *, *, #3610, .F. ) ;
#7752=ORIENTED_EDGE ( 'NONE', *, *, #9207, .F. ) ;
#7769=DIRECTION ( 'NONE',  ( 0.9909299940865187173, -0.1338359446631179062, -0.01207007604876208194 ) ) ;
#7772=CARTESIAN_POINT ( 'NONE',  ( -45.49127566601020334, 166.5779480061062827, 268.8320707926027922 ) ) ;
#7788=AXIS2_PLACEMENT_3D ( 'NONE', #17814, #13887, #15739 ) ;
#7819=ORIENTED_EDGE ( 'NONE', *, *, #18193, .T. ) ;
#7823=CIRCLE ( 'NONE', #16299, 3.047499999999998987 ) ;
#7829=CARTESIAN_POINT ( 'NONE',  ( -41.00000899811524846, 169.5540992312279229, 273.1580453575298293 ) ) ;
#7830=ORIENTED_EDGE ( 'NONE', *, *, #10582, .T. ) ;
#7854=CYLINDRICAL_SURFACE ( 'NONE', #17574, 4.000000000000002665 ) ;
#7880=ORIENTED_EDGE ( 'NONE', *, *, #12390, .T. ) ;
#7912=ORIENTED_EDGE ( 'NONE', *, *, #17252, .T. ) ;
#7968=DIRECTION ( 'NONE',  ( -0.9909299940865188283, 0.1338359446631173788, 0.01207007604876290420 ) ) ;
#7987=CARTESIAN_POINT ( 'NONE',  ( -41.00000899811524846, 169.5540992312279229, 273.1580453575298293 ) ) ;
#8009=DIRECTION ( 'NONE',  ( 0.01292394549866733230, 0.005513023399720419666, 0.9999012842304692006 ) ) ;
#8050=DIRECTION ( 'NONE',  ( 0.9909299940865186063, -0.1338359446631179339, -0.01207007604875938098 ) ) ;
#8065=LINE ( 'NONE', #5790, #3753 ) ;
#8081=PRODUCT ( 'Socket Head Cap Screw', 'Socket Head Cap Screw', '', ( #18380 ) ) ;
#8251=AXIS2_PLACEMENT_3D ( 'NONE', #1488, #1382, #17016 ) ;
#8300=ORIENTED_EDGE ( 'NONE', *, *, #22227, .F. ) ;
#8311=ORIENTED_EDGE ( 'NONE', *, *, #742, .F. ) ;
#8351=COLOUR_RGB ( '', 0.31764706, 0.68627451, 0.89019608) ;
#8466=ADVANCED_FACE ( 'NONE', ( #438 ), #13596, .F. ) ;
#8567=VERTEX_POINT ( 'NONE', #16758 ) ;
#8604=DIRECTION ( 'NONE',  ( 0.01292394549866733230, 0.005513023399720419666, 0.9999012842304692006 ) ) ;
#8660=DIRECTION ( 'NONE',  ( 0.9909299940865190504, -0.1338359446631136318, -0.01207007604876911971 ) ) ;
#8665=VERTEX_POINT ( 'NONE', #6403 ) ;
#8713=AXIS2_PLACEMENT_3D ( 'NONE', #6560, #16806, #8050 ) ;
#8740=DIRECTION ( 'NONE',  ( 0.01292394549866733230, 0.005513023399720419666, 0.9999012842304692006 ) ) ;
#8803=VECTOR ( 'NONE', #16294, 1000.000000000000114 ) ;
#8807=PRODUCT_DEFINITION_FORMATION_WITH_SPECIFIED_SOURCE ( 'ANY', '', #8081, .NOT_KNOWN. ) ;
#8822=DIRECTION ( 'NONE',  ( 0.1337561903331546953, 0.9909881666746205298, -0.007192708699472573526 ) ) ;
#8823=AXIS2_PLACEMENT_3D ( 'NONE', #3730, #3506, #10522 ) ;
#8861=ORIENTED_EDGE ( 'NONE', *, *, #4984, .F. ) ;
#8878=CIRCLE ( 'NONE', #7788, 6.500000000000000000 ) ;
#8941=LINE ( 'NONE', #21122, #10275 ) ;
#8947=CARTESIAN_POINT ( 'NONE',  ( -41.47069032946998846, 166.0668615304125808, 273.1833561390217824 ) ) ;
#8997=FACE_OUTER_BOUND ( 'NONE', #7617, .T. ) ;
#8999=FACE_OUTER_BOUND ( 'NONE', #3443, .T. ) ;
#9027=DIRECTION ( 'NONE',  ( 0.9909299940865190504, -0.1338359446631136318, -0.01207007604876911971 ) ) ;
#9069=FACE_OUTER_BOUND ( 'NONE', #18144, .T. ) ;
#9085=AXIS2_PLACEMENT_3D ( 'NONE', #12787, #13249, #7500 ) ;
#9126=CARTESIAN_POINT ( 'NONE',  ( -38.63447605617402303, 163.9374297322429470, 277.1588331099309812 ) ) ;
#9165=DIRECTION ( 'NONE',  ( -0.01292394549866734098, -0.005513023399720419666, -0.9999012842304692006 ) ) ;
#9178=LINE ( 'NONE', #12661, #10254 ) ;
#9197=CARTESIAN_POINT ( 'NONE',  ( -41.41899454747532161, 166.0889136240114681, 277.1829612759436827 ) ) ;
#9207=EDGE_CURVE ( 'NONE', #12349, #134, #4439, .T. ) ;
#9210=AXIS2_PLACEMENT_3D ( 'NONE', #16701, #20436, #948 ) ;
#9252=DIRECTION ( 'NONE',  ( -0.9250486434174662875, -0.3795887553195633202, 0.01404934683357507604 ) ) ;
#9324=CARTESIAN_POINT ( 'NONE',  ( -41.49342968777003193, 166.0571615038676327, 271.4240548815895977 ) ) ;
#9332=DIRECTION ( 'NONE',  ( 0.01292394549866733404, 0.005513023399720420534, 0.9999012842304693116 ) ) ;
#9346=CARTESIAN_POINT ( 'NONE',  ( -40.94831321612058161, 169.5761513248267818, 277.1576504944517296 ) ) ;
#9356=CARTESIAN_POINT ( 'NONE',  ( -44.25520882077128704, 168.2183454221810734, 273.2074843050344271 ) ) ;
#9369=PLANE ( 'NONE',  #123 ) ;
#9438=ORIENTED_EDGE ( 'NONE', *, *, #15379, .F. ) ;
#9548=DIRECTION ( 'NONE',  ( -0.9250486434174662875, -0.3795887553195633202, 0.01404934683357507604 ) ) ;
#9567=CIRCLE ( 'NONE', #2597, 3.309500000000002107 ) ;
#9594=ORIENTED_EDGE ( 'NONE', *, *, #3870, .T. ) ;
#9621=CARTESIAN_POINT ( 'NONE',  ( -41.94137166082473556, 162.5796238295972671, 273.2086669205137355 ) ) ;
#9669=ORIENTED_EDGE ( 'NONE', *, *, #19556, .T. ) ;
#9689=DIRECTION ( 'NONE',  ( 0.7912924530843117310, -0.6113994113550570431, -0.006856638134102506846 ) ) ;
#9787=CARTESIAN_POINT ( 'NONE',  ( -41.41899454747532161, 166.0889136240114681, 277.1829612759436827 ) ) ;
#9833=AXIS2_PLACEMENT_3D ( 'NONE', #8947, #8604, #12313 ) ;
#9853=CARTESIAN_POINT ( 'NONE',  ( -41.52238611146465530, 166.0448094368136935, 269.1837510020998820 ) ) ;
#9994=ORIENTED_EDGE ( 'NONE', *, *, #17663, .F. ) ;
#10018=DIRECTION ( 'NONE',  ( 0.9909299940865188283, -0.1338359446631172955, -0.01207007604876741101 ) ) ;
#10039=LINE ( 'NONE', #4626, #2619 ) ;
#10092=DIRECTION ( 'NONE',  ( 0.9250486434174662875, 0.3795887553195633202, -0.01404934683357507604 ) ) ;
#10124=ORIENTED_EDGE ( 'NONE', *, *, #19955, .T. ) ;
#10131=LINE ( 'NONE', #20448, #2976 ) ;
#10137=ORIENTED_EDGE ( 'NONE', *, *, #15379, .T. ) ;
#10138=APPLICATION_CONTEXT ( 'automotive_design' ) ;
#10200=VECTOR ( 'NONE', #9332, 999.9999999999998863 ) ;
#10220=ADVANCED_BREP_SHAPE_REPRESENTATION ( '', ( #1915, #6292 ), #7016 ) ;
#10235=EDGE_LOOP ( 'NONE', ( #21055, #2363, #4232, #7159 ) ) ;
#10254=VECTOR ( 'NONE', #16565, 1000.000000000000114 ) ;
#10275=VECTOR ( 'NONE', #8822, 1000.000000000000114 ) ;
#10296=ORIENTED_EDGE ( 'NONE', *, *, #7649, .F. ) ;
#10310=DIRECTION ( 'NONE',  ( -0.3796287383013209893, 0.9251388995215469313, -0.0001940304313831180127 ) ) ;
#10323=AXIS2_PLACEMENT_3D ( 'NONE', #980, #18550, #2808 ) ;
#10378=DIRECTION ( 'NONE',  ( 0.01292394549866733404, 0.005513023399720420534, 0.9999012842304693116 ) ) ;
#10432=LINE ( 'NONE', #20982, #11783 ) ;
#10437=DIRECTION ( 'NONE',  ( 0.9909299940865186063, -0.1338359446631180727, -0.01207007604876311237 ) ) ;
#10522=DIRECTION ( 'NONE',  ( 0.9909299940865187173, -0.1338359446631179062, -0.01207007604876208194 ) ) ;
#10580=DIRECTION ( 'NONE',  ( 0.1337561903331557223, 0.9909881666746205298, -0.007192708699472579598 ) ) ;
#10582=EDGE_CURVE ( 'NONE', #1810, #14816, #12344, .T. ) ;
#10592=EDGE_LOOP ( 'NONE', ( #2217, #6290, #17739, #9438 ) ) ;
#10640=DIRECTION ( 'NONE',  ( 0.9909299940865187173, -0.1338359446631173233, -0.01207007604876291287 ) ) ;
#10679=CARTESIAN_POINT ( 'NONE',  ( -41.94137166082473556, 162.5796238295972671, 273.2086669205137355 ) ) ;
#10716=DIRECTION ( 'NONE',  ( 0.01292394549866734098, 0.005513023399720419666, 0.9999012842304692006 ) ) ;
#10728=EDGE_LOOP ( 'NONE', ( #14108, #20818, #22662, #7079 ) ) ;
#10754=ORIENTED_EDGE ( 'NONE', *, *, #5439, .F. ) ;
#10781=AXIS2_PLACEMENT_3D ( 'NONE', #16042, #17636, #5548 ) ;
#10789=VECTOR ( 'NONE', #10378, 999.9999999999998863 ) ;
#10809=LINE ( 'NONE', #5616, #7623 ) ;
#10846=CARTESIAN_POINT ( 'NONE',  ( -35.08134114990228625, 165.1748757965034144, 269.1052955077829552 ) ) ;
#10884=ORIENTED_EDGE ( 'NONE', *, *, #7383, .F. ) ;
#10888=ORIENTED_EDGE ( 'NONE', *, *, #2365, .T. ) ;
#10943=CIRCLE ( 'NONE', #8713, 5.700000000000001954 ) ;
#10957=VECTOR ( 'NONE', #6464, 999.9999999999998863 ) ;
#11077=LINE ( 'NONE', #9346, #13725 ) ;
#11225=CYLINDRICAL_SURFACE ( 'NONE', #7132, 6.500000000000000000 ) ;
#11259=ORIENTED_EDGE ( 'NONE', *, *, #2400, .F. ) ;
#11292=ORIENTED_EDGE ( 'NONE', *, *, #2056, .T. ) ;
#11311=APPLICATION_CONTEXT ( 'automotive_design' ) ;
#11322=( LENGTH_UNIT ( ) NAMED_UNIT ( * ) SI_UNIT ( .MILLI., .METRE. ) );
#11323=DIRECTION ( 'NONE',  ( 0.01292394549866733230, 0.005513023399720419666, 0.9999012842304692006 ) ) ;
#11373=ORIENTED_EDGE ( 'NONE', *, *, #12494, .T. ) ;
#11388=CARTESIAN_POINT ( 'NONE',  ( -41.52238611146465530, 166.0448094368136935, 269.1837510020998820 ) ) ;
#11394=EDGE_CURVE ( 'NONE', #20004, #13491, #13931, .T. ) ;
#11499=ORIENTED_EDGE ( 'NONE', *, *, #13595, .F. ) ;
#11515=EDGE_LOOP ( 'NONE', ( #5496, #2822 ) ) ;
#11575=ORIENTED_EDGE ( 'NONE', *, *, #7680, .F. ) ;
#11622=CARTESIAN_POINT ( 'NONE',  ( -41.88967587883006871, 162.6016759231961260, 277.2082720574355790 ) ) ;
#11677=DIRECTION ( 'NONE',  ( 0.01292394549866734098, 0.005513023399720419666, 0.9999012842304692006 ) ) ;
#11687=EDGE_LOOP ( 'NONE', ( #16796, #7240 ) ) ;
#11783=VECTOR ( 'NONE', #1371, 999.9999999999998863 ) ;
#11858=VERTEX_POINT ( 'NONE', #10679 ) ;
#11875=ORIENTED_EDGE ( 'NONE', *, *, #11394, .T. ) ;
#11923=VERTEX_POINT ( 'NONE', #21783 ) ;
#12033=PLANE ( 'NONE',  #20148 ) ;
#12069=DIRECTION ( 'NONE',  ( 0.000000000000000000, 0.000000000000000000, 1.000000000000000000 ) ) ;
#12084=VERTEX_POINT ( 'NONE', #16879 ) ;
#12095=EDGE_CURVE ( 'NONE', #8665, #18197, #19591, .T. ) ;
#12192=LINE ( 'NONE', #19290, #4085 ) ;
#12212=DIRECTION ( 'NONE',  ( 0.01292394549866734098, 0.005513023399720419666, 0.9999012842304692006 ) ) ;
#12270=ORIENTED_EDGE ( 'NONE', *, *, #7366, .F. ) ;
#12292=VERTEX_POINT ( 'NONE', #12499 ) ;
#12313=DIRECTION ( 'NONE',  ( 0.9909299940865190504, -0.1338359446631136318, -0.01207007604876911971 ) ) ;
#12344=CIRCLE ( 'NONE', #17865, 4.000000000000002665 ) ;
#12349=VERTEX_POINT ( 'NONE', #7772 ) ;
#12379=CARTESIAN_POINT ( 'NONE',  ( -38.68617183816869698, 163.9153776386440882, 273.1592279730091377 ) ) ;
#12390=EDGE_CURVE ( 'NONE', #6708, #8567, #1242, .T. ) ;
#12421=AXIS2_PLACEMENT_3D ( 'NONE', #9356, #13164, #14553 ) ;
#12444=ADVANCED_FACE ( 'NONE', ( #13306 ), #20387, .T. ) ;
#12482=LINE ( 'NONE', #15493, #21289 ) ;
#12483=ADVANCED_FACE ( 'NONE', ( #2097 ), #14415, .T. ) ;
#12485=VECTOR ( 'NONE', #4477, 1000.000000000000114 ) ;
#12494=EDGE_CURVE ( 'NONE', #21319, #12292, #1992, .T. ) ;
#12499=CARTESIAN_POINT ( 'NONE',  ( -44.49054948644865703, 166.4747265717734308, 273.2201396957804036 ) ) ;
#12552=DIRECTION ( 'NONE',  ( 0.01292394549866734098, 0.005513023399720419666, 0.9999012842304692006 ) ) ;
#12604=SURFACE_SIDE_STYLE ('',( #5571 ) ) ;
#12640=VERTEX_POINT ( 'NONE', #18404 ) ;
#12648=DIRECTION ( 'NONE',  ( -0.9909299940865187173, 0.1338359446631173233, 0.01207007604876291287 ) ) ;
#12649=( NAMED_UNIT ( * ) SI_UNIT ( $, .STERADIAN. ) SOLID_ANGLE_UNIT ( ) );
#12661=CARTESIAN_POINT ( 'NONE',  ( -38.68617183816869698, 163.9153776386440882, 273.1592279730091377 ) ) ;
#12721=LINE ( 'NONE', #7296, #21733 ) ;
#12787=CARTESIAN_POINT ( 'NONE',  ( -41.00000899811524846, 169.5540992312279229, 273.1580453575298293 ) ) ;
#12857=EDGE_LOOP ( 'NONE', ( #17964, #2183, #13195, #15718, #9994, #17568 ) ) ;
#12920=VECTOR ( 'NONE', #12968, 1000.000000000000227 ) ;
#12938=AXIS2_PLACEMENT_3D ( 'NONE', #3570, #6570, #18962 ) ;
#12952=LINE ( 'NONE', #18319, #15096 ) ;
#12956=DIRECTION ( 'NONE',  ( 0.7912924530843116200, -0.6113994113550571541, -0.006856638134102505111 ) ) ;
#12968=DIRECTION ( 'NONE',  ( -0.7912924530843117310, 0.6113994113550571541, 0.006856638134102506846 ) ) ;
#12974=ADVANCED_FACE ( 'NONE', ( #17315 ), #22550, .T. ) ;
#13053=LINE ( 'NONE', #21835, #5495 ) ;
#13058=ORIENTED_EDGE ( 'NONE', *, *, #1695, .T. ) ;
#13074=FACE_BOUND ( 'NONE', #13941, .T. ) ;
#13119=DIRECTION ( 'NONE',  ( 0.9909299940865186063, -0.1338359446631180727, -0.01207007604876311237 ) ) ;
#13160=ADVANCED_FACE ( 'NONE', ( #14105 ), #21087, .F. ) ;
#13164=DIRECTION ( 'NONE',  ( -0.9909299940865189393, 0.1338359446631160188, 0.01207007604876292328 ) ) ;
#13190=LINE ( 'NONE', #9621, #12920 ) ;
#13195=ORIENTED_EDGE ( 'NONE', *, *, #21158, .T. ) ;
#13235=TOROIDAL_SURFACE ( 'NONE', #4016, 4.400000000000000355, 0.4000000000000000222 ) ;
#13249=DIRECTION ( 'NONE',  ( -0.6113012557851977835, -0.7913029548584309403, 0.01226410648014603956 ) ) ;
#13287=CIRCLE ( 'NONE', #5914, 5.700000000000001954 ) ;
#13293=DIRECTION ( 'NONE',  ( 0.9909299940865190504, -0.1338359446631136318, -0.01207007604876911971 ) ) ;
#13306=FACE_OUTER_BOUND ( 'NONE', #7018, .T. ) ;
#13320=AXIS2_PLACEMENT_3D ( 'NONE', #14562, #11323, #2594 ) ;
#13349=DIRECTION ( 'NONE',  ( 0.01292394549866733404, 0.005513023399720420534, 0.9999012842304693116 ) ) ;
#13362=DIRECTION ( 'NONE',  ( -0.9909299940865186063, 0.1338359446631179339, 0.01207007604875938098 ) ) ;
#13369=CARTESIAN_POINT ( 'NONE',  ( -41.00865927789263310, 166.2639521169525665, 308.9298270502609967 ) ) ;
#13380=DIRECTION ( 'NONE',  ( 0.7098319280015313870, -0.09073800780701757329, 0.6985021459729685578 ) ) ;
#13440=ORIENTED_EDGE ( 'NONE', *, *, #22227, .T. ) ;
#13461=ADVANCED_FACE ( 'NONE', ( #8997 ), #21280, .T. ) ;
#13481=CARTESIAN_POINT ( 'NONE',  ( -38.21549050681395698, 167.4026153394593734, 273.1339171915171846 ) ) ;
#13491=VERTEX_POINT ( 'NONE', #21396 ) ;
#13595=EDGE_CURVE ( 'NONE', #12084, #18692, #6362, .T. ) ;
#13596=CONICAL_SURFACE ( 'NONE', #21625, 3.047499999999998987, 1.047197551196594523 ) ;
#13602=DIRECTION ( 'NONE',  ( -0.9250486434174662875, -0.3795887553195633202, 0.01404934683357507604 ) ) ;
#13671=DIRECTION ( 'NONE',  ( 0.01292394549866733230, 0.005513023399720419666, 0.9999012842304692006 ) ) ;
#13673=AXIS2_PLACEMENT_3D ( 'NONE', #21422, #14564, #7633 ) ;
#13674=CARTESIAN_POINT ( 'NONE',  ( -45.80028074091057988, 166.4461343731306613, 244.9249310372943285 ) ) ;
#13725=VECTOR ( 'NONE', #14891, 1000.000000000000227 ) ;
#13772=VERTEX_POINT ( 'NONE', #21108 ) ;
#13794=ORIENTED_EDGE ( 'NONE', *, *, #16537, .T. ) ;
#13804=ORIENTED_EDGE ( 'NONE', *, *, #12095, .T. ) ;
#13821=CARTESIAN_POINT ( 'NONE',  ( -44.25520882077128704, 168.2183454221810734, 273.2074843050344271 ) ) ;
#13852=AXIS2_PLACEMENT_3D ( 'NONE', #9853, #8009, #13955 ) ;
#13887=DIRECTION ( 'NONE',  ( 0.01292394549866733230, 0.005513023399720419666, 0.9999012842304692006 ) ) ;
#13912=VECTOR ( 'NONE', #14844, 1000.000000000000114 ) ;
#13917=ORIENTED_EDGE ( 'NONE', *, *, #16711, .F. ) ;
#13931=LINE ( 'NONE', #19547, #10789 ) ;
#13941=EDGE_LOOP ( 'NONE', ( #4493, #19111 ) ) ;
#13955=DIRECTION ( 'NONE',  ( 0.9909299940865187173, -0.1338359446631179062, -0.01207007604876208194 ) ) ;
#14026=( NAMED_UNIT ( * ) PLANE_ANGLE_UNIT ( ) SI_UNIT ( $, .RADIAN. ) );
#14048=CARTESIAN_POINT ( 'NONE',  ( -37.16746371568343932, 165.4537260709361135, 268.7306821537931683 ) ) ;
#14072=ORIENTED_EDGE ( 'NONE', *, *, #832, .T. ) ;
#14105=FACE_OUTER_BOUND ( 'NONE', #18195, .T. ) ;
#14108=ORIENTED_EDGE ( 'NONE', *, *, #16537, .F. ) ;
#14136=DIRECTION ( 'NONE',  ( 0.01292394549866733230, 0.005513023399720419666, 0.9999012842304692006 ) ) ;
#14332=FILL_AREA_STYLE ('',( #7293 ) ) ;
#14339=ORIENTED_EDGE ( 'NONE', *, *, #3771, .F. ) ;
#14398=DIRECTION ( 'NONE',  ( -0.9910138020846641638, 0.1337596504095987238, 0.000000000000000000 ) ) ;
#14415=PLANE ( 'NONE',  #19153 ) ;
#14553=DIRECTION ( 'NONE',  ( 0.1337561903331544733, 0.9909881666746205298, -0.007192708699472569189 ) ) ;
#14560=DIRECTION ( 'NONE',  ( 0.01292394549866733404, 0.005513023399720420534, 0.9999012842304693116 ) ) ;
#14562=CARTESIAN_POINT ( 'NONE',  ( -41.00865927789263310, 166.2639521169525665, 308.9298270502609967 ) ) ;
#14564=DIRECTION ( 'NONE',  ( 0.01292394549866733230, 0.005513023399720419666, 0.9999012842304692006 ) ) ;
#14616=ORIENTED_EDGE ( 'NONE', *, *, #12095, .F. ) ;
#14624=CIRCLE ( 'NONE', #19349, 4.399999999999996803 ) ;
#14726=EDGE_CURVE ( 'NONE', #12292, #8665, #2391, .T. ) ;
#14740=CONICAL_SURFACE ( 'NONE', #9210, 3.047499999999998987, 1.047197551196594523 ) ;
#14769=VERTEX_POINT ( 'NONE', #4575 ) ;
#14798=( NAMED_UNIT ( * ) PLANE_ANGLE_UNIT ( ) SI_UNIT ( $, .RADIAN. ) );
#14816=VERTEX_POINT ( 'NONE', #13674 ) ;
#14823=CARTESIAN_POINT ( 'NONE',  ( -38.45083117249132698, 165.6589964890517592, 273.1465725822631612 ) ) ;
#14844=DIRECTION ( 'NONE',  ( -0.6915547089979457995, 0.09853460026858232301, 0.7155718112200041281 ) ) ;
#14878=EDGE_CURVE ( 'NONE', #3984, #18513, #8878, .T. ) ;
#14885=EDGE_LOOP ( 'NONE', ( #16590, #6875, #17230, #7752 ) ) ;
#14888=CARTESIAN_POINT ( 'NONE',  ( -41.00865927789263310, 166.2639521169525665, 308.9298270502609967 ) ) ;
#14891=DIRECTION ( 'NONE',  ( -0.9250486434174662875, -0.3795887553195633202, 0.01404934683357507604 ) ) ;
#14914=SHAPE_REPRESENTATION ( 'Socket Head Cap Screw', ( #6292 ), #7016 ) ;
#14929=PLANE ( 'NONE',  #5171 ) ;
#15040=LINE ( 'NONE', #14823, #21364 ) ;
#15096=VECTOR ( 'NONE', #16506, 1000.000000000000000 ) ;
#15102=DIRECTION ( 'NONE',  ( 0.9909299940865188283, -0.1338359446631172955, -0.01207007604876741101 ) ) ;
#15379=EDGE_CURVE ( 'NONE', #2284, #18513, #12482, .T. ) ;
#15386=CARTESIAN_POINT ( 'NONE',  ( -38.68617183816869698, 163.9153776386440882, 273.1592279730091377 ) ) ;
#15429=EDGE_CURVE ( 'NONE', #18692, #13491, #17893, .T. ) ;
#15435=EDGE_CURVE ( 'NONE', #14816, #12349, #16399, .T. ) ;
#15484=EDGE_CURVE ( 'NONE', #13772, #12349, #20932, .T. ) ;
#15492=AXIS2_PLACEMENT_3D ( 'NONE', #14048, #10580, #14398 ) ;
#15493=CARTESIAN_POINT ( 'NONE',  ( -34.56761431633026405, 165.3940184766423158, 308.8513715559440698 ) ) ;
#15507=VECTOR ( 'NONE', #16358, 1000.000000000000000 ) ;
#15540=FACE_OUTER_BOUND ( 'NONE', #22219, .T. ) ;
#15569=VECTOR ( 'NONE', #968, 999.9999999999998863 ) ;
#15614=DIRECTION ( 'NONE',  ( 0.9909299940865190504, -0.1338359446631136318, -0.01207007604876911971 ) ) ;
#15698=ORIENTED_EDGE ( 'NONE', *, *, #22096, .T. ) ;
#15718=ORIENTED_EDGE ( 'NONE', *, *, #21561, .T. ) ;
#15728=CARTESIAN_POINT ( 'NONE',  ( -41.00000899811524846, 169.5540992312279229, 273.1580453575298293 ) ) ;
#15738=DIRECTION ( 'NONE',  ( 0.9909299940865187173, -0.1338359446631179062, -0.01207007604876208194 ) ) ;
#15739=DIRECTION ( 'NONE',  ( 0.9909299940865187173, -0.1338359446631179062, -0.01207007604876208194 ) ) ;
#15757=DIRECTION ( 'NONE',  ( -0.7098319280015157329, 0.09073800780701535285, -0.6985021459729847670 ) ) ;
#15799=AXIS2_PLACEMENT_3D ( 'NONE', #9787, #17032, #13362 ) ;
#15830=AXIS2_PLACEMENT_3D ( 'NONE', #20883, #3542, #1824 ) ;
#15857=EDGE_CURVE ( 'NONE', #7115, #11923, #9567, .T. ) ;
#15922=UNCERTAINTY_MEASURE_WITH_UNIT (LENGTH_MEASURE( 1.000000000000000082E-05 ), #11322, 'distance_accuracy_value', 'NONE');
#15985=EDGE_LOOP ( 'NONE', ( #270, #11292, #18571 ) ) ;
#16042=CARTESIAN_POINT ( 'NONE',  ( -38.21549050681395698, 167.4026153394593734, 273.1339171915171846 ) ) ;
#16092=AXIS2_PLACEMENT_3D ( 'NONE', #4653, #22442, #8660 ) ;
#16104=( GEOMETRIC_REPRESENTATION_CONTEXT ( 3 ) GLOBAL_UNCERTAINTY_ASSIGNED_CONTEXT ( ( #15922 ) ) GLOBAL_UNIT_ASSIGNED_CONTEXT ( ( #11322, #14798, #21854 ) ) REPRESENTATION_CONTEXT ( 'NONE', 'WORKASPACE' ) );
#16119=LINE ( 'NONE', #361, #1212 ) ;
#16123=EDGE_CURVE ( 'NONE', #160, #2284, #21651, .T. ) ;
#16142=ORIENTED_EDGE ( 'NONE', *, *, #17663, .T. ) ;
#16147=CLOSED_SHELL ( 'NONE', ( #22639, #4117, #17875, #20816, #16757, #437, #22398, #16858, #17217, #4270, #19474, #18491, #19776, #17542, #3723, #13160, #5716, #19609, #4012, #7098, #13461, #7306, #12974, #4973, #12444, #12483, #8466 ) ) ;
#16170=FACE_OUTER_BOUND ( 'NONE', #20960, .T. ) ;
#16258=CIRCLE ( 'NONE', #12938, 4.000000000000002665 ) ;
#16270=CARTESIAN_POINT ( 'NONE',  ( -47.06729551376846388, 166.8517785085912237, 277.2517607094216032 ) ) ;
#16290=ORIENTED_EDGE ( 'NONE', *, *, #19221, .F. ) ;
#16294=DIRECTION ( 'NONE',  ( 0.1337561903331546953, 0.9909881666746205298, -0.007192708699472573526 ) ) ;
#16299=AXIS2_PLACEMENT_3D ( 'NONE', #16511, #18128, #13293 ) ;
#16353=ORIENTED_EDGE ( 'NONE', *, *, #19556, .F. ) ;
#16358=DIRECTION ( 'NONE',  ( 0.6915547089979297013, -0.09853460026858011644, -0.7155718112200200043 ) ) ;
#16399=LINE ( 'NONE', #7414, #402 ) ;
#16429=VECTOR ( 'NONE', #19954, 1000.000000000000227 ) ;
#16480=VECTOR ( 'NONE', #21062, 1000.000000000000000 ) ;
#16506=DIRECTION ( 'NONE',  ( 0.7912924530843117310, -0.6113994113550570431, -0.006856638134102506846 ) ) ;
#16511=CARTESIAN_POINT ( 'NONE',  ( -41.47069032946998846, 166.0668615304125808, 273.1833561390217824 ) ) ;
#16537=EDGE_CURVE ( 'NONE', #17163, #7184, #13287, .T. ) ;
#16565=DIRECTION ( 'NONE',  ( 0.1337561903331546953, 0.9909881666746205298, -0.007192708699472573526 ) ) ;
#16590=ORIENTED_EDGE ( 'NONE', *, *, #15484, .F. ) ;
#16701=CARTESIAN_POINT ( 'NONE',  ( -41.47069032946998846, 166.0668615304125808, 273.1833561390217824 ) ) ;
#16711=EDGE_CURVE ( 'NONE', #18167, #20021, #10131, .T. ) ;
#16757=ADVANCED_FACE ( 'NONE', ( #15540 ), #6351, .T. ) ;
#16758=CARTESIAN_POINT ( 'NONE',  ( -40.94831321612058161, 169.5761513248267818, 277.1576504944517296 ) ) ;
#16776=ORIENTED_EDGE ( 'NONE', *, *, #6717, .F. ) ;
#16796=ORIENTED_EDGE ( 'NONE', *, *, #19044, .F. ) ;
#16806=DIRECTION ( 'NONE',  ( 0.01292394549866733230, 0.005513023399720419666, 0.9999012842304692006 ) ) ;
#16858=ADVANCED_FACE ( 'NONE', ( #17269 ), #5062, .T. ) ;
#16879=CARTESIAN_POINT ( 'NONE',  ( -38.68617183816869698, 163.9153776386440882, 273.1592279730091377 ) ) ;
#16966=VECTOR ( 'NONE', #21474, 1000.000000000000227 ) ;
#17016=DIRECTION ( 'NONE',  ( 0.9909299940865190504, -0.1338359446631136318, -0.01207007604876911971 ) ) ;
#17032=DIRECTION ( 'NONE',  ( -0.01292394549866733230, -0.005513023399720419666, -0.9999012842304692006 ) ) ;
#17111=DIRECTION ( 'NONE',  ( 0.01292394549866733230, 0.005513023399720419666, 0.9999012842304692006 ) ) ;
#17129=LINE ( 'NONE', #6549, #416 ) ;
#17141=CARTESIAN_POINT ( 'NONE',  ( -41.00000899811524846, 169.5540992312279229, 273.1580453575298293 ) ) ;
#17163=VERTEX_POINT ( 'NONE', #6472 ) ;
#17193=CARTESIAN_POINT ( 'NONE',  ( -38.21549050681395698, 167.4026153394593734, 273.1339171915171846 ) ) ;
#17217=ADVANCED_FACE ( 'NONE', ( #20238 ), #1924, .T. ) ;
#17230=ORIENTED_EDGE ( 'NONE', *, *, #1363, .F. ) ;
#17252=EDGE_CURVE ( 'NONE', #11923, #1810, #8065, .T. ) ;
#17269=FACE_OUTER_BOUND ( 'NONE', #11687, .T. ) ;
#17281=ORIENTED_EDGE ( 'NONE', *, *, #3771, .T. ) ;
#17308=ORIENTED_EDGE ( 'NONE', *, *, #1657, .T. ) ;
#17312=DIRECTION ( 'NONE',  ( 0.01292394549866733404, 0.005513023399720420534, 0.9999012842304693116 ) ) ;
#17315=FACE_OUTER_BOUND ( 'NONE', #15985, .T. ) ;
#17333=AXIS2_PLACEMENT_3D ( 'NONE', #6682, #1416, #22499 ) ;
#17435=DIRECTION ( 'NONE',  ( 0.9909299940865190504, -0.1338359446631162408, -0.01207007604876292155 ) ) ;
#17469=CARTESIAN_POINT ( 'NONE',  ( -41.83656076456451700, 165.9107905944781862, 244.8766507330992681 ) ) ;
#17539=ORIENTED_EDGE ( 'NONE', *, *, #14726, .T. ) ;
#17542=ADVANCED_FACE ( 'NONE', ( #8999 ), #13235, .F. ) ;
#17568=ORIENTED_EDGE ( 'NONE', *, *, #19955, .F. ) ;
#17574=AXIS2_PLACEMENT_3D ( 'NONE', #14888, #21830, #15102 ) ;
#17596=CIRCLE ( 'NONE', #19407, 6.500000000000000000 ) ;
#17636=DIRECTION ( 'NONE',  ( 0.01292394549866734098, 0.005513023399720419666, 0.9999012842304692006 ) ) ;
#17649=CIRCLE ( 'NONE', #15830, 3.047499999999998987 ) ;
#17663=EDGE_CURVE ( 'NONE', #14769, #12640, #13053, .T. ) ;
#17730=CIRCLE ( 'NONE', #2684, 3.309500000000002107 ) ;
#17739=ORIENTED_EDGE ( 'NONE', *, *, #2894, .F. ) ;
#17814=CARTESIAN_POINT ( 'NONE',  ( -41.42933370387425640, 166.0845032052916963, 276.3830402485593254 ) ) ;
#17865=AXIS2_PLACEMENT_3D ( 'NONE', #17469, #3317, #21005 ) ;
#17875=ADVANCED_FACE ( 'NONE', ( #3106 ), #2932, .T. ) ;
#17893=LINE ( 'NONE', #9126, #8803 ) ;
#17946=EDGE_LOOP ( 'NONE', ( #5008, #20091, #9669, #15698, #9594 ) ) ;
#17964=ORIENTED_EDGE ( 'NONE', *, *, #18029, .T. ) ;
#17976=EDGE_LOOP ( 'NONE', ( #7730, #22455, #10137, #4547 ) ) ;
#17998=ORIENTED_EDGE ( 'NONE', *, *, #2591, .T. ) ;
#18029=EDGE_CURVE ( 'NONE', #8567, #13491, #17129, .T. ) ;
#18116=DIRECTION ( 'NONE',  ( -0.01292394549866733230, -0.005513023399720419666, -0.9999012842304692006 ) ) ;
#18128=DIRECTION ( 'NONE',  ( 0.01292394549866733230, 0.005513023399720419666, 0.9999012842304692006 ) ) ;
#18144=EDGE_LOOP ( 'NONE', ( #19306, #5137, #3957, #3323 ) ) ;
#18167=VERTEX_POINT ( 'NONE', #1834 ) ;
#18176=CARTESIAN_POINT ( 'NONE',  ( -35.77069358118216513, 165.3260487394316840, 277.1141618424657054 ) ) ;
#18179=CARTESIAN_POINT ( 'NONE',  ( -41.84548474893134085, 165.9069838518206836, 244.1862188963381755 ) ) ;
#18193=EDGE_CURVE ( 'NONE', #7184, #3984, #12192, .T. ) ;
#18194=CARTESIAN_POINT ( 'NONE',  ( -47.44970423945500926, 167.1338857572628456, 309.0082825445779804 ) ) ;
#18195=EDGE_LOOP ( 'NONE', ( #7560, #3520, #3299, #8311, #4808 ) ) ;
#18197=VERTEX_POINT ( 'NONE', #1620 ) ;
#18210=DIRECTION ( 'NONE',  ( -0.1337561903331544455, -0.9909881666746205298, 0.007192708699472569189 ) ) ;
#18228=PLANE ( 'NONE',  #500 ) ;
#18234=DIRECTION ( 'NONE',  ( 0.01292394549866733230, 0.005513023399720419666, 0.9999012842304692006 ) ) ;
#18319=CARTESIAN_POINT ( 'NONE',  ( -41.00000899811524846, 169.5540992312279229, 273.1580453575298293 ) ) ;
#18380=PRODUCT_CONTEXT ( 'NONE', #10138, 'mechanical' ) ;
#18404=CARTESIAN_POINT ( 'NONE',  ( -44.67419437013135308, 164.7531598149646470, 277.2324002234482236 ) ) ;
#18460=VECTOR ( 'NONE', #4647, 999.9999999999998863 ) ;
#18491=ADVANCED_FACE ( 'NONE', ( #6150 ), #4294, .T. ) ;
#18513=VERTEX_POINT ( 'NONE', #2818 ) ;
#18534=FACE_OUTER_BOUND ( 'NONE', #10235, .T. ) ;
#18550=DIRECTION ( 'NONE',  ( -0.1337561903331558333, -0.9909881666746205298, 0.007192708699472581332 ) ) ;
#18571=ORIENTED_EDGE ( 'NONE', *, *, #7074, .F. ) ;
#18610=VERTEX_POINT ( 'NONE', #1229 ) ;
#18631=ORIENTED_EDGE ( 'NONE', *, *, #12390, .F. ) ;
#18692=VERTEX_POINT ( 'NONE', #2308 ) ;
#18779=CARTESIAN_POINT ( 'NONE',  ( -41.41899454747532161, 166.0889136240114681, 277.1829612759436827 ) ) ;
#18825=SHAPE_DEFINITION_REPRESENTATION ( #751, #14914 ) ;
#18853=CARTESIAN_POINT ( 'NONE',  ( -37.04493930154655601, 165.7286083383001198, 308.8815467460659647 ) ) ;
#18954=DIRECTION ( 'NONE',  ( -0.9250486434174662875, -0.3795887553195633202, 0.01404934683357507604 ) ) ;
#18962=DIRECTION ( 'NONE',  ( 0.9909299940865188283, -0.1338359446631172955, -0.01207007604876047212 ) ) ;
#18984=EDGE_LOOP ( 'NONE', ( #17281, #13794 ) ) ;
#19044=EDGE_CURVE ( 'NONE', #11923, #7115, #17730, .T. ) ;
#19111=ORIENTED_EDGE ( 'NONE', *, *, #4984, .T. ) ;
#19153=AXIS2_PLACEMENT_3D ( 'NONE', #19553, #10716, #30 ) ;
#19171=( LENGTH_UNIT ( ) NAMED_UNIT ( * ) SI_UNIT ( .MILLI., .METRE. ) );
#19214=DIRECTION ( 'NONE',  ( 0.9909299940865186063, -0.1338359446631179339, -0.01207007604875938098 ) ) ;
#19221=EDGE_CURVE ( 'NONE', #21319, #21410, #15040, .T. ) ;
#19290=CARTESIAN_POINT ( 'NONE',  ( -47.06729551376847809, 166.8517785085912237, 277.2517607094216032 ) ) ;
#19306=ORIENTED_EDGE ( 'NONE', *, *, #19044, .T. ) ;
#19331=EDGE_CURVE ( 'NONE', #12084, #18197, #12721, .T. ) ;
#19349=AXIS2_PLACEMENT_3D ( 'NONE', #11388, #950, #21921 ) ;
#19358=DIRECTION ( 'NONE',  ( -0.1337561903331546953, -0.9909881666746205298, 0.007192708699472573526 ) ) ;
#19384=AXIS2_PLACEMENT_3D ( 'NONE', #2468, #18116, #7968 ) ;
#19407=AXIS2_PLACEMENT_3D ( 'NONE', #6644, #13671, #15738 ) ;
#19474=ADVANCED_FACE ( 'NONE', ( #13074, #2820 ), #18228, .T. ) ;
#19502=AXIS2_PLACEMENT_3D ( 'NONE', #459, #9165, #12648 ) ;
#19515=ORIENTED_EDGE ( 'NONE', *, *, #21659, .F. ) ;
#19547=CARTESIAN_POINT ( 'NONE',  ( -38.21549050681395698, 167.4026153394593734, 273.1339171915171846 ) ) ;
#19553=CARTESIAN_POINT ( 'NONE',  ( -38.21549050681395698, 167.4026153394593734, 273.1339171915171846 ) ) ;
#19556=EDGE_CURVE ( 'NONE', #21410, #5718, #7823, .T. ) ;
#19585=SURFACE_STYLE_USAGE ( .BOTH. , #12604 ) ;
#19589=CARTESIAN_POINT ( 'NONE',  ( -41.52238611146465530, 166.0448094368136935, 269.1837510020998820 ) ) ;
#19591=CIRCLE ( 'NONE', #3467, 3.047499999999998987 ) ;
#19609=ADVANCED_FACE ( 'NONE', ( #2378 ), #9369, .T. ) ;
#19688=EDGE_LOOP ( 'NONE', ( #21011, #18631, #10888, #13440, #11875 ) ) ;
#19768=AXIS2_PLACEMENT_3D ( 'NONE', #19589, #7194, #2253 ) ;
#19776=ADVANCED_FACE ( 'NONE', ( #4744 ), #5618, .T. ) ;
#19861=CIRCLE ( 'NONE', #17333, 4.000000000000002665 ) ;
#19954=DIRECTION ( 'NONE',  ( -0.7912924530843117310, 0.6113994113550571541, 0.006856638134102506846 ) ) ;
#19955=EDGE_CURVE ( 'NONE', #8567, #14769, #11077, .T. ) ;
#20004=VERTEX_POINT ( 'NONE', #2900 ) ;
#20021=VERTEX_POINT ( 'NONE', #13821 ) ;
#20065=LINE ( 'NONE', #5714, #16429 ) ;
#20091=ORIENTED_EDGE ( 'NONE', *, *, #19221, .T. ) ;
#20104=PLANE ( 'NONE',  #9085 ) ;
#20148=AXIS2_PLACEMENT_3D ( 'NONE', #15386, #10310, #10092 ) ;
#20238=FACE_OUTER_BOUND ( 'NONE', #21874, .T. ) ;
#20277=DIRECTION ( 'NONE',  ( 0.9909299940865187173, -0.1338359446631173233, -0.01207007604876291287 ) ) ;
#20347=DIRECTION ( 'NONE',  ( 0.01292394549866733230, 0.005513023399720419666, 0.9999012842304692006 ) ) ;
#20387=PLANE ( 'NONE',  #1222 ) ;
#20436=DIRECTION ( 'NONE',  ( 0.01292394549866733230, 0.005513023399720419666, 0.9999012842304692006 ) ) ;
#20448=CARTESIAN_POINT ( 'NONE',  ( -41.00000899811524846, 169.5540992312279229, 273.1580453575298293 ) ) ;
#20563=LINE ( 'NONE', #17141, #21569 ) ;
#20755=ORIENTED_EDGE ( 'NONE', *, *, #832, .F. ) ;
#20807=ORIENTED_EDGE ( 'NONE', *, *, #5396, .F. ) ;
#20816=ADVANCED_FACE ( 'NONE', ( #4199 ), #11225, .T. ) ;
#20818=ORIENTED_EDGE ( 'NONE', *, *, #7649, .T. ) ;
#20844=CONICAL_SURFACE ( 'NONE', #21928, 3.309500000000002107, 0.7853981633974710386 ) ;
#20883=CARTESIAN_POINT ( 'NONE',  ( -41.47069032946998846, 166.0668615304125808, 273.1833561390217824 ) ) ;
#20923=EDGE_LOOP ( 'NONE', ( #22156, #19515, #14072, #22217, #21542 ) ) ;
#20932=CIRCLE ( 'NONE', #1850, 4.000000000000002665 ) ;
#20960=EDGE_LOOP ( 'NONE', ( #16142, #16776, #2572, #6116, #1460 ) ) ;
#20982=CARTESIAN_POINT ( 'NONE',  ( -44.72589015212603414, 164.7311077213657597, 273.2327950865263801 ) ) ;
#21005=DIRECTION ( 'NONE',  ( 0.9909299940865188283, -0.1338359446631172955, -0.01207007604876047212 ) ) ;
#21011=ORIENTED_EDGE ( 'NONE', *, *, #18029, .F. ) ;
#21055=ORIENTED_EDGE ( 'NONE', *, *, #15435, .F. ) ;
#21062=DIRECTION ( 'NONE',  ( -0.1337561903331544455, -0.9909881666746205298, 0.007192708699472569189 ) ) ;
#21080=ORIENTED_EDGE ( 'NONE', *, *, #21659, .T. ) ;
#21087=PLANE ( 'NONE',  #6003 ) ;
#21108=CARTESIAN_POINT ( 'NONE',  ( -37.56383571331804916, 165.5072604488013326, 268.7355101842127283 ) ) ;
#21114=DIRECTION ( 'NONE',  ( 0.9909299940865186063, -0.1338359446631180727, -0.01207007604876311237 ) ) ;
#21115=CARTESIAN_POINT ( 'NONE',  ( -47.96343107302703146, 166.9147430771239442, 269.2622064964168658 ) ) ;
#21122=CARTESIAN_POINT ( 'NONE',  ( -38.68617183816869698, 163.9153776386440882, 273.1592279730091377 ) ) ;
#21158=EDGE_CURVE ( 'NONE', #18692, #1423, #10039, .T. ) ;
#21190=EDGE_LOOP ( 'NONE', ( #14616, #20755, #10754 ) ) ;
#21252=PLANE ( 'NONE',  #7728 ) ;
#21261=DIRECTION ( 'NONE',  ( -0.8517085755015534332, 0.1186618397176080614, 0.5104036345990761170 ) ) ;
#21280=PLANE ( 'NONE',  #10781 ) ;
#21289=VECTOR ( 'NONE', #17312, 999.9999999999998863 ) ;
#21319=VERTEX_POINT ( 'NONE', #9324 ) ;
#21345=SHAPE_REPRESENTATION_RELATIONSHIP ( 'NONE' , 'NONE' ,  #14914, #10220 ) ;
#21364=VECTOR ( 'NONE', #4555, 1000.000000000000114 ) ;
#21366=VECTOR ( 'NONE', #21261, 1000.000000000000114 ) ;
#21396=CARTESIAN_POINT ( 'NONE',  ( -38.16379472481928303, 167.4246674330582891, 277.1335223284390850 ) ) ;
#21410=VERTEX_POINT ( 'NONE', #735 ) ;
#21419=DIRECTION ( 'NONE',  ( -0.01292394549866733230, -0.005513023399720419666, -0.9999012842304692006 ) ) ;
#21422=CARTESIAN_POINT ( 'NONE',  ( -41.84548474893134085, 165.9069838518206836, 244.1862188963381755 ) ) ;
#21474=DIRECTION ( 'NONE',  ( -0.7912924530843117310, 0.6113994113550571541, 0.006856638134102506846 ) ) ;
#21542=ORIENTED_EDGE ( 'NONE', *, *, #6717, .T. ) ;
#21561=EDGE_CURVE ( 'NONE', #1423, #12640, #1743, .T. ) ;
#21569=VECTOR ( 'NONE', #9689, 1000.000000000000000 ) ;
#21625=AXIS2_PLACEMENT_3D ( 'NONE', #320, #3763, #9027 ) ;
#21632=DIRECTION ( 'NONE',  ( 0.6113012557851978945, 0.7913029548584308293, -0.01226410648014603956 ) ) ;
#21651=CIRCLE ( 'NONE', #8823, 6.500000000000000000 ) ;
#21659=EDGE_CURVE ( 'NONE', #11858, #1423, #5735, .T. ) ;
#21670=EDGE_CURVE ( 'NONE', #13772, #18610, #1188, .T. ) ;
#21677=UNCERTAINTY_MEASURE_WITH_UNIT (LENGTH_MEASURE( 1.000000000000000082E-05 ), #19171, 'distance_accuracy_value', 'NONE');
#21733=VECTOR ( 'NONE', #9252, 1000.000000000000114 ) ;
#21773=PRODUCT_DEFINITION ( 'UNKNOWN', '', #8807, #22549 ) ;
#21783=CARTESIAN_POINT ( 'NONE',  ( -38.56600193350200811, 165.4640537929580830, 244.1462729796548103 ) ) ;
#21807=FACE_OUTER_BOUND ( 'NONE', #1329, .T. ) ;
#21830=DIRECTION ( 'NONE',  ( 0.01292394549866733230, 0.005513023399720419666, 0.9999012842304692006 ) ) ;
#21835=CARTESIAN_POINT ( 'NONE',  ( -44.20351303877662019, 168.2403975157799607, 277.2070894419563274 ) ) ;
#21854=( NAMED_UNIT ( * ) SI_UNIT ( $, .STERADIAN. ) SOLID_ANGLE_UNIT ( ) );
#21857=DIRECTION ( 'NONE',  ( -0.9909299940865187173, 0.1338359446631173233, 0.01207007604876291287 ) ) ;
#21874=EDGE_LOOP ( 'NONE', ( #2887, #3567, #7912, #10884 ) ) ;
#21886=EDGE_LOOP ( 'NONE', ( #5952, #11499, #4078, #3905, #21080 ) ) ;
#21895=CIRCLE ( 'NONE', #9833, 3.047499999999998987 ) ;
#21917=LINE ( 'NONE', #6209, #12485 ) ;
#21921=DIRECTION ( 'NONE',  ( -0.9909299940865182732, 0.1338359446631206262, 0.01207007604876868950 ) ) ;
#21928=AXIS2_PLACEMENT_3D ( 'NONE', #18179, #6093, #13119 ) ;
#22016=LINE ( 'NONE', #22136, #13912 ) ;
#22096=EDGE_CURVE ( 'NONE', #5718, #18167, #17649, .T. ) ;
#22122=CARTESIAN_POINT ( 'NONE',  ( -41.47069032946998846, 166.0668615304125808, 273.1833561390217824 ) ) ;
#22136=CARTESIAN_POINT ( 'NONE',  ( -45.12496756436068068, 166.3499139106832558, 244.2261648130215690 ) ) ;
#22154=LINE ( 'NONE', #7829, #3272 ) ;
#22156=ORIENTED_EDGE ( 'NONE', *, *, #21561, .F. ) ;
#22217=ORIENTED_EDGE ( 'NONE', *, *, #7074, .T. ) ;
#22219=EDGE_LOOP ( 'NONE', ( #7830, #1054, #6028, #11259 ) ) ;
#22227=EDGE_CURVE ( 'NONE', #5718, #20004, #12952, .T. ) ;
#22291=CIRCLE ( 'NONE', #16092, 3.047499999999998987 ) ;
#22398=ADVANCED_FACE ( 'NONE', ( #2092, #2436 ), #21252, .T. ) ;
#22424=VECTOR ( 'NONE', #7020, 999.9999999999998863 ) ;
#22442=DIRECTION ( 'NONE',  ( 0.01292394549866733230, 0.005513023399720419666, 0.9999012842304692006 ) ) ;
#22455=ORIENTED_EDGE ( 'NONE', *, *, #16123, .T. ) ;
#22459=AXIS2_PLACEMENT_3D ( 'NONE', #17193, #1466, #4999 ) ;
#22499=DIRECTION ( 'NONE',  ( -0.9909299940865188283, 0.1338359446631172955, 0.01207007604876741101 ) ) ;
#22549=PRODUCT_DEFINITION_CONTEXT ( 'detailed design', #11311, 'design' ) ;
#22550=PLANE ( 'NONE',  #22459 ) ;
#22639=ADVANCED_FACE ( 'NONE', ( #21807 ), #14740, .F. ) ;
#22662=ORIENTED_EDGE ( 'NONE', *, *, #2894, .T. ) ;
ENDSEC;
END-ISO-10303-21;
